ISO-10303-21;
HEADER;
/* Generated by software containing ST-Developer
 * from STEP Tools, Inc. (www.steptools.com) 
 */

FILE_DESCRIPTION(
/* description */ ('PAT-091'),
/* implementation_level */ '2;1');

FILE_NAME(
/* name */ 'Cap Screw - M5x20.step',
/* time_stamp */ '2026-10-27T15:34:44-07:00',
/* author */ (''),
/* organization */ (''),
/* preprocessor_version */ 'ST-DEVELOPER v20.2',
/* originating_system */ 'Autodesk Translation Framework v15.17.0.0',
/* authorisation */ '');

FILE_SCHEMA (('AUTOMOTIVE_DESIGN { 1 0 10303 214 3 1 1 }'));
ENDSEC;

DATA;
#10=MECHANICAL_DESIGN_GEOMETRIC_PRESENTATION_REPRESENTATION('',(#1001),#25100);
#732=CONICAL_SURFACE('',#15095,0.4,0.785398163397448);
#733=CONICAL_SURFACE('',#15099,0.41,0.785398163397448);
#734=CONICAL_SURFACE('',#15103,0.26,0.463647609000806);
#735=CONICAL_SURFACE('',#15107,0.225,0.785398163397448);
#746=ORIENTED_CLOSED_SHELL('',*,#13280,.F.);
#749=BREP_WITH_VOIDS('Body1',#13279,(#746));
#781=SHAPE_REPRESENTATION_RELATIONSHIP('SRR','None',#25543,#891);
#891=ADVANCED_BREP_SHAPE_REPRESENTATION('',(#749),#25013);
#1001=STYLED_ITEM('',(#26198),#749);
#1391=FACE_BOUND('',#3305,.T.);
#1766=PLANE('',#15093);
#1767=PLANE('',#15101);
#1768=PLANE('',#15109);
#1769=PLANE('',#15110);
#1770=PLANE('',#15111);
#1771=PLANE('',#15112);
#1772=PLANE('',#15113);
#1773=PLANE('',#15114);
#1774=PLANE('',#15115);
#1775=PLANE('',#15116);
#1776=PLANE('',#15117);
#2306=FACE_OUTER_BOUND('',#3300,.T.);
#2307=FACE_OUTER_BOUND('',#3301,.T.);
#2308=FACE_OUTER_BOUND('',#3302,.T.);
#2309=FACE_OUTER_BOUND('',#3303,.T.);
#2310=FACE_OUTER_BOUND('',#3304,.T.);
#2311=FACE_OUTER_BOUND('',#3306,.T.);
#2312=FACE_OUTER_BOUND('',#3307,.T.);
#2313=FACE_OUTER_BOUND('',#3308,.T.);
#2314=FACE_OUTER_BOUND('',#3309,.T.);
#2315=FACE_OUTER_BOUND('',#3310,.T.);
#2316=FACE_OUTER_BOUND('',#3311,.T.);
#2317=FACE_OUTER_BOUND('',#3312,.T.);
#2318=FACE_OUTER_BOUND('',#3313,.T.);
#2319=FACE_OUTER_BOUND('',#3314,.T.);
#2320=FACE_OUTER_BOUND('',#3315,.T.);
#2321=FACE_OUTER_BOUND('',#3316,.T.);
#2322=FACE_OUTER_BOUND('',#3317,.T.);
#3300=EDGE_LOOP('',(#9992));
#3301=EDGE_LOOP('',(#9993,#9994,#9995,#9996));
#3302=EDGE_LOOP('',(#9997,#9998,#9999,#10000));
#3303=EDGE_LOOP('',(#10001,#10002,#10003,#10004));
#3304=EDGE_LOOP('',(#10005));
#3305=EDGE_LOOP('',(#10006));
#3306=EDGE_LOOP('',(#10007,#10008,#10009,#10010));
#3307=EDGE_LOOP('',(#10011,#10012,#10013,#10014));
#3308=EDGE_LOOP('',(#10015,#10016,#10017,#10018));
#3309=EDGE_LOOP('',(#10019));
#3310=EDGE_LOOP('',(#10020,#10021,#10022,#10023));
#3311=EDGE_LOOP('',(#10024,#10025,#10026,#10027));
#3312=EDGE_LOOP('',(#10028,#10029,#10030,#10031));
#3313=EDGE_LOOP('',(#10032,#10033,#10034,#10035));
#3314=EDGE_LOOP('',(#10036,#10037,#10038,#10039));
#3315=EDGE_LOOP('',(#10040,#10041,#10042,#10043));
#3316=EDGE_LOOP('',(#10044,#10045,#10046,#10047,#10048,#10049));
#3317=EDGE_LOOP('',(#10050,#10051,#10052,#10053,#10054,#10055));
#4403=LINE('',#22106,#5143);
#4404=LINE('',#22110,#5144);
#4405=LINE('',#22114,#5145);
#4406=LINE('',#22121,#5146);
#4407=LINE('',#22125,#5147);
#4408=LINE('',#22129,#5148);
#4409=LINE('',#22134,#5149);
#4410=LINE('',#22136,#5150);
#4411=LINE('',#22138,#5151);
#4412=LINE('',#22139,#5152);
#4413=LINE('',#22142,#5153);
#4414=LINE('',#22144,#5154);
#4415=LINE('',#22145,#5155);
#4416=LINE('',#22148,#5156);
#4417=LINE('',#22150,#5157);
#4418=LINE('',#22151,#5158);
#4419=LINE('',#22154,#5159);
#4420=LINE('',#22156,#5160);
#4421=LINE('',#22157,#5161);
#4422=LINE('',#22160,#5162);
#4423=LINE('',#22162,#5163);
#4424=LINE('',#22163,#5164);
#4425=LINE('',#22165,#5165);
#4426=LINE('',#22166,#5166);
#5143=VECTOR('',#17771,0.4);
#5144=VECTOR('',#17776,0.425);
#5145=VECTOR('',#17781,0.41);
#5146=VECTOR('',#17790,0.26);
#5147=VECTOR('',#17795,0.25);
#5148=VECTOR('',#17800,0.225);
#5149=VECTOR('',#17805,1.);
#5150=VECTOR('',#17806,1.);
#5151=VECTOR('',#17807,1.);
#5152=VECTOR('',#17808,1.);
#5153=VECTOR('',#17811,1.);
#5154=VECTOR('',#17812,1.);
#5155=VECTOR('',#17813,1.);
#5156=VECTOR('',#17816,1.);
#5157=VECTOR('',#17817,1.);
#5158=VECTOR('',#17818,1.);
#5159=VECTOR('',#17821,1.);
#5160=VECTOR('',#17822,1.);
#5161=VECTOR('',#17823,1.);
#5162=VECTOR('',#17826,1.);
#5163=VECTOR('',#17827,1.);
#5164=VECTOR('',#17828,1.);
#5165=VECTOR('',#17831,1.);
#5166=VECTOR('',#17832,1.);
#5835=CIRCLE('',#15094,0.375);
#5836=CIRCLE('',#15096,0.425);
#5837=CIRCLE('',#15098,0.425);
#5838=CIRCLE('',#15100,0.395);
#5839=CIRCLE('',#15102,0.27);
#5840=CIRCLE('',#15104,0.24505);
#5841=CIRCLE('',#15106,0.24505);
#5842=CIRCLE('',#15108,0.2);
#6722=VERTEX_POINT('',#22101);
#6723=VERTEX_POINT('',#22104);
#6724=VERTEX_POINT('',#22108);
#6725=VERTEX_POINT('',#22112);
#6726=VERTEX_POINT('',#22116);
#6727=VERTEX_POINT('',#22119);
#6728=VERTEX_POINT('',#22123);
#6729=VERTEX_POINT('',#22127);
#6730=VERTEX_POINT('',#22132);
#6731=VERTEX_POINT('',#22133);
#6732=VERTEX_POINT('',#22135);
#6733=VERTEX_POINT('',#22137);
#6734=VERTEX_POINT('',#22141);
#6735=VERTEX_POINT('',#22143);
#6736=VERTEX_POINT('',#22147);
#6737=VERTEX_POINT('',#22149);
#6738=VERTEX_POINT('',#22153);
#6739=VERTEX_POINT('',#22155);
#6740=VERTEX_POINT('',#22159);
#6741=VERTEX_POINT('',#22161);
#7931=EDGE_CURVE('',#6722,#6722,#5835,.T.);
#7932=EDGE_CURVE('',#6723,#6723,#5836,.T.);
#7933=EDGE_CURVE('',#6723,#6722,#4403,.T.);
#7934=EDGE_CURVE('',#6724,#6724,#5837,.T.);
#7935=EDGE_CURVE('',#6724,#6723,#4404,.T.);
#7936=EDGE_CURVE('',#6725,#6725,#5838,.T.);
#7937=EDGE_CURVE('',#6725,#6724,#4405,.T.);
#7938=EDGE_CURVE('',#6726,#6726,#5839,.T.);
#7939=EDGE_CURVE('',#6727,#6727,#5840,.F.);
#7940=EDGE_CURVE('',#6727,#6726,#4406,.T.);
#7941=EDGE_CURVE('',#6728,#6728,#5841,.F.);
#7942=EDGE_CURVE('',#6728,#6727,#4407,.T.);
#7943=EDGE_CURVE('',#6729,#6729,#5842,.T.);
#7944=EDGE_CURVE('',#6729,#6728,#4408,.T.);
#7945=EDGE_CURVE('',#6730,#6731,#4409,.T.);
#7946=EDGE_CURVE('',#6731,#6732,#4410,.T.);
#7947=EDGE_CURVE('',#6732,#6733,#4411,.T.);
#7948=EDGE_CURVE('',#6730,#6733,#4412,.T.);
#7949=EDGE_CURVE('',#6731,#6734,#4413,.T.);
#7950=EDGE_CURVE('',#6734,#6735,#4414,.T.);
#7951=EDGE_CURVE('',#6735,#6732,#4415,.T.);
#7952=EDGE_CURVE('',#6734,#6736,#4416,.T.);
#7953=EDGE_CURVE('',#6736,#6737,#4417,.T.);
#7954=EDGE_CURVE('',#6737,#6735,#4418,.T.);
#7955=EDGE_CURVE('',#6736,#6738,#4419,.T.);
#7956=EDGE_CURVE('',#6738,#6739,#4420,.T.);
#7957=EDGE_CURVE('',#6739,#6737,#4421,.T.);
#7958=EDGE_CURVE('',#6738,#6740,#4422,.T.);
#7959=EDGE_CURVE('',#6740,#6741,#4423,.T.);
#7960=EDGE_CURVE('',#6741,#6739,#4424,.T.);
#7961=EDGE_CURVE('',#6740,#6730,#4425,.T.);
#7962=EDGE_CURVE('',#6733,#6741,#4426,.T.);
#9992=ORIENTED_EDGE('',*,*,#7931,.F.);
#9993=ORIENTED_EDGE('',*,*,#7932,.F.);
#9994=ORIENTED_EDGE('',*,*,#7933,.T.);
#9995=ORIENTED_EDGE('',*,*,#7931,.T.);
#9996=ORIENTED_EDGE('',*,*,#7933,.F.);
#9997=ORIENTED_EDGE('',*,*,#7934,.F.);
#9998=ORIENTED_EDGE('',*,*,#7935,.T.);
#9999=ORIENTED_EDGE('',*,*,#7932,.T.);
#10000=ORIENTED_EDGE('',*,*,#7935,.F.);
#10001=ORIENTED_EDGE('',*,*,#7936,.F.);
#10002=ORIENTED_EDGE('',*,*,#7937,.T.);
#10003=ORIENTED_EDGE('',*,*,#7934,.T.);
#10004=ORIENTED_EDGE('',*,*,#7937,.F.);
#10005=ORIENTED_EDGE('',*,*,#7936,.T.);
#10006=ORIENTED_EDGE('',*,*,#7938,.F.);
#10007=ORIENTED_EDGE('',*,*,#7939,.F.);
#10008=ORIENTED_EDGE('',*,*,#7940,.T.);
#10009=ORIENTED_EDGE('',*,*,#7938,.T.);
#10010=ORIENTED_EDGE('',*,*,#7940,.F.);
#10011=ORIENTED_EDGE('',*,*,#7941,.F.);
#10012=ORIENTED_EDGE('',*,*,#7942,.T.);
#10013=ORIENTED_EDGE('',*,*,#7939,.T.);
#10014=ORIENTED_EDGE('',*,*,#7942,.F.);
#10015=ORIENTED_EDGE('',*,*,#7943,.F.);
#10016=ORIENTED_EDGE('',*,*,#7944,.T.);
#10017=ORIENTED_EDGE('',*,*,#7941,.T.);
#10018=ORIENTED_EDGE('',*,*,#7944,.F.);
#10019=ORIENTED_EDGE('',*,*,#7943,.T.);
#10020=ORIENTED_EDGE('',*,*,#7945,.T.);
#10021=ORIENTED_EDGE('',*,*,#7946,.T.);
#10022=ORIENTED_EDGE('',*,*,#7947,.T.);
#10023=ORIENTED_EDGE('',*,*,#7948,.F.);
#10024=ORIENTED_EDGE('',*,*,#7949,.T.);
#10025=ORIENTED_EDGE('',*,*,#7950,.T.);
#10026=ORIENTED_EDGE('',*,*,#7951,.T.);
#10027=ORIENTED_EDGE('',*,*,#7946,.F.);
#10028=ORIENTED_EDGE('',*,*,#7952,.T.);
#10029=ORIENTED_EDGE('',*,*,#7953,.T.);
#10030=ORIENTED_EDGE('',*,*,#7954,.T.);
#10031=ORIENTED_EDGE('',*,*,#7950,.F.);
#10032=ORIENTED_EDGE('',*,*,#7955,.T.);
#10033=ORIENTED_EDGE('',*,*,#7956,.T.);
#10034=ORIENTED_EDGE('',*,*,#7957,.T.);
#10035=ORIENTED_EDGE('',*,*,#7953,.F.);
#10036=ORIENTED_EDGE('',*,*,#7958,.T.);
#10037=ORIENTED_EDGE('',*,*,#7959,.T.);
#10038=ORIENTED_EDGE('',*,*,#7960,.T.);
#10039=ORIENTED_EDGE('',*,*,#7956,.F.);
#10040=ORIENTED_EDGE('',*,*,#7961,.T.);
#10041=ORIENTED_EDGE('',*,*,#7948,.T.);
#10042=ORIENTED_EDGE('',*,*,#7962,.T.);
#10043=ORIENTED_EDGE('',*,*,#7959,.F.);
#10044=ORIENTED_EDGE('',*,*,#7961,.F.);
#10045=ORIENTED_EDGE('',*,*,#7958,.F.);
#10046=ORIENTED_EDGE('',*,*,#7955,.F.);
#10047=ORIENTED_EDGE('',*,*,#7952,.F.);
#10048=ORIENTED_EDGE('',*,*,#7949,.F.);
#10049=ORIENTED_EDGE('',*,*,#7945,.F.);
#10050=ORIENTED_EDGE('',*,*,#7962,.F.);
#10051=ORIENTED_EDGE('',*,*,#7947,.F.);
#10052=ORIENTED_EDGE('',*,*,#7951,.F.);
#10053=ORIENTED_EDGE('',*,*,#7954,.F.);
#10054=ORIENTED_EDGE('',*,*,#7957,.F.);
#10055=ORIENTED_EDGE('',*,*,#7960,.F.);
#12188=CYLINDRICAL_SURFACE('',#15097,0.425);
#12189=CYLINDRICAL_SURFACE('',#15105,0.24505);
#12673=ADVANCED_FACE('',(#2306),#1766,.T.);
#12674=ADVANCED_FACE('',(#2307),#732,.T.);
#12675=ADVANCED_FACE('',(#2308),#12188,.T.);
#12676=ADVANCED_FACE('',(#2309),#733,.T.);
#12677=ADVANCED_FACE('',(#2310,#1391),#1767,.T.);
#12678=ADVANCED_FACE('',(#2311),#734,.T.);
#12679=ADVANCED_FACE('',(#2312),#12189,.T.);
#12680=ADVANCED_FACE('',(#2313),#735,.T.);
#12681=ADVANCED_FACE('',(#2314),#1768,.T.);
#12682=ADVANCED_FACE('',(#2315),#1769,.F.);
#12683=ADVANCED_FACE('',(#2316),#1770,.F.);
#12684=ADVANCED_FACE('',(#2317),#1771,.F.);
#12685=ADVANCED_FACE('',(#2318),#1772,.F.);
#12686=ADVANCED_FACE('',(#2319),#1773,.F.);
#12687=ADVANCED_FACE('',(#2320),#1774,.F.);
#12688=ADVANCED_FACE('',(#2321),#1775,.F.);
#12689=ADVANCED_FACE('',(#2322),#1776,.F.);
#13279=CLOSED_SHELL('',(#12673,#12674,#12675,#12676,#12677,#12678,#12679,
#12680,#12681));
#13280=CLOSED_SHELL('',(#12682,#12683,#12684,#12685,#12686,#12687,#12688,
#12689));
#15092=AXIS2_PLACEMENT_3D('',#22099,#17761,#17762);
#15093=AXIS2_PLACEMENT_3D('',#22100,#17763,#17764);
#15094=AXIS2_PLACEMENT_3D('',#22102,#17765,#17766);
#15095=AXIS2_PLACEMENT_3D('',#22103,#17767,#17768);
#15096=AXIS2_PLACEMENT_3D('',#22105,#17769,#17770);
#15097=AXIS2_PLACEMENT_3D('',#22107,#17772,#17773);
#15098=AXIS2_PLACEMENT_3D('',#22109,#17774,#17775);
#15099=AXIS2_PLACEMENT_3D('',#22111,#17777,#17778);
#15100=AXIS2_PLACEMENT_3D('',#22113,#17779,#17780);
#15101=AXIS2_PLACEMENT_3D('',#22115,#17782,#17783);
#15102=AXIS2_PLACEMENT_3D('',#22117,#17784,#17785);
#15103=AXIS2_PLACEMENT_3D('',#22118,#17786,#17787);
#15104=AXIS2_PLACEMENT_3D('',#22120,#17788,#17789);
#15105=AXIS2_PLACEMENT_3D('',#22122,#17791,#17792);
#15106=AXIS2_PLACEMENT_3D('',#22124,#17793,#17794);
#15107=AXIS2_PLACEMENT_3D('',#22126,#17796,#17797);
#15108=AXIS2_PLACEMENT_3D('',#22128,#17798,#17799);
#15109=AXIS2_PLACEMENT_3D('',#22130,#17801,#17802);
#15110=AXIS2_PLACEMENT_3D('',#22131,#17803,#17804);
#15111=AXIS2_PLACEMENT_3D('',#22140,#17809,#17810);
#15112=AXIS2_PLACEMENT_3D('',#22146,#17814,#17815);
#15113=AXIS2_PLACEMENT_3D('',#22152,#17819,#17820);
#15114=AXIS2_PLACEMENT_3D('',#22158,#17824,#17825);
#15115=AXIS2_PLACEMENT_3D('',#22164,#17829,#17830);
#15116=AXIS2_PLACEMENT_3D('',#22167,#17833,#17834);
#15117=AXIS2_PLACEMENT_3D('',#22168,#17835,#17836);
#17761=DIRECTION('axis',(0.,0.,1.));
#17762=DIRECTION('refdir',(1.,0.,0.));
#17763=DIRECTION('center_axis',(0.,1.,0.));
#17764=DIRECTION('ref_axis',(0.,0.,1.));
#17765=DIRECTION('center_axis',(0.,-1.,0.));
#17766=DIRECTION('ref_axis',(1.,0.,0.));
#17767=DIRECTION('center_axis',(0.,-1.,0.));
#17768=DIRECTION('ref_axis',(1.,0.,0.));
#17769=DIRECTION('center_axis',(0.,-1.,0.));
#17770=DIRECTION('ref_axis',(1.,0.,0.));
#17771=DIRECTION('',(0.707106781186548,0.707106781186547,8.65956056235493E-17));
#17772=DIRECTION('center_axis',(0.,-1.,0.));
#17773=DIRECTION('ref_axis',(1.,0.,0.));
#17774=DIRECTION('center_axis',(0.,-1.,0.));
#17775=DIRECTION('ref_axis',(1.,0.,0.));
#17776=DIRECTION('',(0.,1.,0.));
#17777=DIRECTION('center_axis',(0.,1.,0.));
#17778=DIRECTION('ref_axis',(1.,0.,0.));
#17779=DIRECTION('center_axis',(0.,-1.,0.));
#17780=DIRECTION('ref_axis',(1.,0.,0.));
#17781=DIRECTION('',(-0.707106781186547,0.707106781186548,-8.65956056235493E-17));
#17782=DIRECTION('center_axis',(0.,-1.,0.));
#17783=DIRECTION('ref_axis',(0.,0.,-1.));
#17784=DIRECTION('center_axis',(0.,-1.,0.));
#17785=DIRECTION('ref_axis',(1.,0.,0.));
#17786=DIRECTION('center_axis',(0.,1.,0.));
#17787=DIRECTION('ref_axis',(1.,0.,0.));
#17788=DIRECTION('center_axis',(0.,1.,0.));
#17789=DIRECTION('ref_axis',(1.,0.,0.));
#17790=DIRECTION('',(-0.447213595499958,0.894427190999916,-5.47678698264203E-17));
#17791=DIRECTION('center_axis',(0.,-1.,0.));
#17792=DIRECTION('ref_axis',(1.,0.,0.));
#17793=DIRECTION('center_axis',(0.,1.,0.));
#17794=DIRECTION('ref_axis',(1.,0.,0.));
#17795=DIRECTION('',(0.,1.,0.));
#17796=DIRECTION('center_axis',(0.,1.,0.));
#17797=DIRECTION('ref_axis',(1.,0.,0.));
#17798=DIRECTION('center_axis',(0.,-1.,0.));
#17799=DIRECTION('ref_axis',(1.,0.,0.));
#17800=DIRECTION('',(-0.707106781186547,0.707106781186548,-8.65956056235493E-17));
#17801=DIRECTION('center_axis',(0.,-1.,0.));
#17802=DIRECTION('ref_axis',(0.,0.,-1.));
#17803=DIRECTION('center_axis',(0.866025403784439,0.,-0.5));
#17804=DIRECTION('ref_axis',(0.5,0.,0.866025403784439));
#17805=DIRECTION('',(-0.5,0.,-0.866025403784439));
#17806=DIRECTION('',(0.,-1.,0.));
#17807=DIRECTION('',(0.5,0.,0.866025403784439));
#17808=DIRECTION('',(0.,-1.,0.));
#17809=DIRECTION('center_axis',(1.20185167898973E-16,0.,-1.));
#17810=DIRECTION('ref_axis',(1.,0.,1.20185167898973E-16));
#17811=DIRECTION('',(-1.,0.,-1.20185167898973E-16));
#17812=DIRECTION('',(0.,-1.,0.));
#17813=DIRECTION('',(1.,0.,1.20185167898973E-16));
#17814=DIRECTION('center_axis',(-0.866025403784439,0.,-0.5));
#17815=DIRECTION('ref_axis',(0.5,0.,-0.866025403784439));
#17816=DIRECTION('',(-0.5,0.,0.866025403784439));
#17817=DIRECTION('',(0.,-1.,0.));
#17818=DIRECTION('',(0.5,0.,-0.866025403784439));
#17819=DIRECTION('center_axis',(-0.866025403784439,0.,0.5));
#17820=DIRECTION('ref_axis',(-0.5,0.,-0.866025403784439));
#17821=DIRECTION('',(0.5,0.,0.866025403784439));
#17822=DIRECTION('',(0.,-1.,0.));
#17823=DIRECTION('',(-0.5,0.,-0.866025403784439));
#17824=DIRECTION('center_axis',(-2.40370335797945E-16,0.,1.));
#17825=DIRECTION('ref_axis',(-1.,0.,-2.40370335797945E-16));
#17826=DIRECTION('',(1.,0.,2.40370335797945E-16));
#17827=DIRECTION('',(0.,-1.,0.));
#17828=DIRECTION('',(-1.,0.,-2.40370335797945E-16));
#17829=DIRECTION('center_axis',(0.866025403784439,0.,0.5));
#17830=DIRECTION('ref_axis',(-0.5,0.,0.866025403784439));
#17831=DIRECTION('',(0.5,0.,-0.866025403784439));
#17832=DIRECTION('',(-0.5,0.,0.866025403784439));
#17833=DIRECTION('center_axis',(0.,1.,0.));
#17834=DIRECTION('ref_axis',(1.,0.,0.));
#17835=DIRECTION('center_axis',(0.,-1.,0.));
#17836=DIRECTION('ref_axis',(0.,0.,-1.));
#22099=CARTESIAN_POINT('',(0.,0.,0.));
#22100=CARTESIAN_POINT('Origin',(0.375,0.5,0.));
#22101=CARTESIAN_POINT('',(-0.375,0.5,-4.59242549680257E-17));
#22102=CARTESIAN_POINT('Origin',(0.,0.5,0.));
#22103=CARTESIAN_POINT('Origin',(0.,0.475,0.));
#22104=CARTESIAN_POINT('',(-0.425,0.45,-5.20474889637625E-17));
#22105=CARTESIAN_POINT('Origin',(0.,0.45,0.));
#22106=CARTESIAN_POINT('',(-0.4,0.475,-4.89858719658941E-17));
#22107=CARTESIAN_POINT('Origin',(0.,0.24,0.));
#22108=CARTESIAN_POINT('',(-0.425,0.0299999999999998,-5.20474889637625E-17));
#22109=CARTESIAN_POINT('Origin',(0.,0.0299999999999998,0.));
#22110=CARTESIAN_POINT('',(-0.425,0.24,-5.20474889637625E-17));
#22111=CARTESIAN_POINT('Origin',(0.,0.0150000000000001,0.));
#22112=CARTESIAN_POINT('',(-0.395,4.85722573273506E-17,-4.83735485663204E-17));
#22113=CARTESIAN_POINT('Origin',(0.,0.,0.));
#22114=CARTESIAN_POINT('',(-0.41,0.0150000000000001,-5.02105187650415E-17));
#22115=CARTESIAN_POINT('Origin',(0.27,0.,0.));
#22116=CARTESIAN_POINT('',(-0.27,0.,-3.30654635769785E-17));
#22117=CARTESIAN_POINT('Origin',(0.,0.,0.));
#22118=CARTESIAN_POINT('Origin',(0.,-0.02,0.));
#22119=CARTESIAN_POINT('',(-0.24505,-0.0498999999999999,3.00099698131059E-17));
#22120=CARTESIAN_POINT('Origin',(0.,-0.0498999999999999,0.));
#22121=CARTESIAN_POINT('',(-0.26,-0.02,-3.18408167778312E-17));
#22122=CARTESIAN_POINT('Origin',(0.,-0.995,0.));
#22123=CARTESIAN_POINT('',(-0.24505,-1.95495,3.00099698131059E-17));
#22124=CARTESIAN_POINT('Origin',(0.,-1.95495,0.));
#22125=CARTESIAN_POINT('',(-0.24505,-0.995,-3.00099698131059E-17));
#22126=CARTESIAN_POINT('Origin',(0.,-1.975,0.));
#22127=CARTESIAN_POINT('',(-0.2,-2.,-2.44929359829471E-17));
#22128=CARTESIAN_POINT('Origin',(0.,-2.,0.));
#22129=CARTESIAN_POINT('',(-0.225,-1.975,-2.75545529808154E-17));
#22130=CARTESIAN_POINT('Origin',(0.,-2.,0.));
#22131=CARTESIAN_POINT('Origin',(0.115470053837925,-0.5,-0.2));
#22132=CARTESIAN_POINT('',(0.23094010767585,-0.5,0.));
#22133=CARTESIAN_POINT('',(0.115470053837925,-0.5,-0.2));
#22134=CARTESIAN_POINT('',(0.23094010767585,-0.5,0.));
#22135=CARTESIAN_POINT('',(0.115470053837925,-0.8,-0.2));
#22136=CARTESIAN_POINT('',(0.115470053837925,-0.5,-0.2));
#22137=CARTESIAN_POINT('',(0.23094010767585,-0.8,0.));
#22138=CARTESIAN_POINT('',(0.23094010767585,-0.8,0.));
#22139=CARTESIAN_POINT('',(0.23094010767585,-0.5,0.));
#22140=CARTESIAN_POINT('Origin',(-0.115470053837925,-0.5,-0.2));
#22141=CARTESIAN_POINT('',(-0.115470053837925,-0.5,-0.2));
#22142=CARTESIAN_POINT('',(0.115470053837925,-0.5,-0.2));
#22143=CARTESIAN_POINT('',(-0.115470053837925,-0.8,-0.2));
#22144=CARTESIAN_POINT('',(-0.115470053837925,-0.5,-0.2));
#22145=CARTESIAN_POINT('',(0.115470053837925,-0.8,-0.2));
#22146=CARTESIAN_POINT('Origin',(-0.23094010767585,-0.5,-2.77555756156289E-17));
#22147=CARTESIAN_POINT('',(-0.23094010767585,-0.5,-2.82820063659975E-17));
#22148=CARTESIAN_POINT('',(-0.115470053837925,-0.5,-0.2));
#22149=CARTESIAN_POINT('',(-0.23094010767585,-0.8,-2.77555756156289E-17));
#22150=CARTESIAN_POINT('',(-0.23094010767585,-0.5,-2.82820063659975E-17));
#22151=CARTESIAN_POINT('',(-0.115470053837925,-0.8,-0.2));
#22152=CARTESIAN_POINT('Origin',(-0.115470053837925,-0.5,0.2));
#22153=CARTESIAN_POINT('',(-0.115470053837925,-0.5,0.2));
#22154=CARTESIAN_POINT('',(-0.23094010767585,-0.5,-2.82820063659975E-17));
#22155=CARTESIAN_POINT('',(-0.115470053837925,-0.8,0.2));
#22156=CARTESIAN_POINT('',(-0.115470053837925,-0.5,0.2));
#22157=CARTESIAN_POINT('',(-0.23094010767585,-0.8,-2.82820063659975E-17));
#22158=CARTESIAN_POINT('Origin',(0.115470053837925,-0.5,0.2));
#22159=CARTESIAN_POINT('',(0.115470053837925,-0.5,0.2));
#22160=CARTESIAN_POINT('',(-0.115470053837925,-0.5,0.2));
#22161=CARTESIAN_POINT('',(0.115470053837925,-0.8,0.2));
#22162=CARTESIAN_POINT('',(0.115470053837925,-0.5,0.2));
#22163=CARTESIAN_POINT('',(-0.115470053837925,-0.8,0.2));
#22164=CARTESIAN_POINT('Origin',(0.23094010767585,-0.5,0.));
#22165=CARTESIAN_POINT('',(0.115470053837925,-0.5,0.2));
#22166=CARTESIAN_POINT('',(0.115470053837925,-0.8,0.2));
#22167=CARTESIAN_POINT('Origin',(0.,-0.5,0.));
#22168=CARTESIAN_POINT('Origin',(0.,-0.8,0.));
#24892=UNCERTAINTY_MEASURE_WITH_UNIT(LENGTH_MEASURE(0.001),#25101,
'DISTANCE_ACCURACY_VALUE',
'Maximum model space distance between geometric entities at asserted c
onnectivities');
#24979=UNCERTAINTY_MEASURE_WITH_UNIT(LENGTH_MEASURE(0.001),#25101,
'DISTANCE_ACCURACY_VALUE',
'Maximum model space distance between geometric entities at asserted c
onnectivities');
#25013=(
GEOMETRIC_REPRESENTATION_CONTEXT(3)
GLOBAL_UNCERTAINTY_ASSIGNED_CONTEXT((#24892))
GLOBAL_UNIT_ASSIGNED_CONTEXT((#25101,#25103,#25104))
REPRESENTATION_CONTEXT('','3D')
);
#25100=(
GEOMETRIC_REPRESENTATION_CONTEXT(3)
GLOBAL_UNCERTAINTY_ASSIGNED_CONTEXT((#24979))
GLOBAL_UNIT_ASSIGNED_CONTEXT((#25101,#25103,#25104))
REPRESENTATION_CONTEXT('','3D')
);
#25101=(
LENGTH_UNIT()
NAMED_UNIT(*)
SI_UNIT(.CENTI.,.METRE.)
);
#25103=(
NAMED_UNIT(*)
PLANE_ANGLE_UNIT()
SI_UNIT($,.RADIAN.)
);
#25104=(
NAMED_UNIT(*)
SI_UNIT($,.STERADIAN.)
SOLID_ANGLE_UNIT()
);
#25138=SHAPE_DEFINITION_REPRESENTATION(#25258,#25543);
#25258=PRODUCT_DEFINITION_SHAPE('',$,#25664);
#25543=SHAPE_REPRESENTATION('',(#15092),#25013);
#25630=PRODUCT_DEFINITION_CONTEXT('part definition',#25992,'design');
#25664=PRODUCT_DEFINITION('Cap Screw - M5x20','Cap Screw - M5x20',#25784,
#25630);
#25784=PRODUCT_DEFINITION_FORMATION('',$,#26027);
#25992=APPLICATION_CONTEXT(
'Core Data for Automotive Mechanical Design Process');
#25993=PRODUCT_CONTEXT('part definition',#25992,'mechanical');
#26027=PRODUCT('Cap Screw - M5x20','Cap Screw - M5x20',
'Cap Screw - M5x20',(#25993));
#26192=COLOUR_RGB('Black',0.12,0.14,0.17);
#26193=FILL_AREA_STYLE_COLOUR('',#26192);
#26194=FILL_AREA_STYLE('',(#26193));
#26195=SURFACE_STYLE_FILL_AREA(#26194);
#26196=SURFACE_SIDE_STYLE('',(#26195));
#26197=SURFACE_STYLE_USAGE(.BOTH.,#26196);
#26198=PRESENTATION_STYLE_ASSIGNMENT((#26197));
ENDSEC;
END-ISO-10303-21;
